ISO-10303-21;
HEADER;
FILE_DESCRIPTION (('STEP AP214'),
    '1' );
FILE_NAME ('Angle Locking Side Clamp.step',
    '2026-10-09T10:51:02',
    ( '' ),
    ( '' ),
    'SwSTEP 2.0',
    'SolidWorks 2026',
    '' );
FILE_SCHEMA (( 'AUTOMOTIVE_DESIGN' ));
ENDSEC;

DATA;
#53=CARTESIAN_POINT ( 'NONE',  ( 83.22761354253117361, 75.14843460673597519, -6.385946070498853544 ) ) ;
#75=DIRECTION ( 'NONE',  ( 0.9999164797902018176, 2.001050586498093021E-22, -0.01292414190464117804 ) ) ;
#244=ADVANCED_FACE ( 'NONE', ( #2899 ), #1200, .F. ) ;
#282=CARTESIAN_POINT ( 'NONE',  ( 76.11837255219295173, 75.12984171660241373, -5.954615140807677953 ) ) ;
#355=SHAPE_DEFINITION_REPRESENTATION ( #14203, #21889 ) ;
#398=CARTESIAN_POINT ( 'NONE',  ( 79.50704247290580895, 75.20582465103802861, -7.278313778469502893 ) ) ;
#442=CARTESIAN_POINT ( 'NONE',  ( 2.775557561562891351E-13, 184.8436277385793289, 3.707971429900425164E-14 ) ) ;
#448=AXIS2_PLACEMENT_3D ( 'NONE', #13092, #19825, #9504 ) ;
#461=CARTESIAN_POINT ( 'NONE',  ( 51.64670511766545502, 84.99999999999997158, -27.66980033337678790 ) ) ;
#519=VECTOR ( 'NONE', #22182, 1000.000000000000000 ) ;
#524=ADVANCED_FACE ( 'NONE', ( #20667 ), #8478, .T. ) ;
#539=CARTESIAN_POINT ( 'NONE',  ( 79.65664043722195231, 75.20579285942561398, 5.220605708544542978 ) ) ;
#558=VERTEX_POINT ( 'NONE', #9880 ) ;
#705=DIRECTION ( 'NONE',  ( -7.176269450075762180E-19, 1.000000000000000000, -5.550596000020001457E-17 ) ) ;
#866=DIRECTION ( 'NONE',  ( 0.9999164797902015955, 2.001050586498092550E-22, -0.01292414190464117457 ) ) ;
#1002=DIRECTION ( 'NONE',  ( -7.176269450075762180E-19, 1.000000000000000000, -5.550596000020001457E-17 ) ) ;
#1016=LINE ( 'NONE', #8010, #8056 ) ;
#1075=CARTESIAN_POINT ( 'NONE',  ( 79.99331838321640475, 74.99899999999998101, -1.033931352371301404 ) ) ;
#1160=ORIENTED_EDGE ( 'NONE', *, *, #8863, .T. ) ;
#1200=CYLINDRICAL_SURFACE ( 'NONE', #8339, 6.250000000000000000 ) ;
#1217=VERTEX_POINT ( 'NONE', #5644 ) ;
#1230=CARTESIAN_POINT ( 'NONE',  ( 81.68308784690056257, 75.19231584242493227, 4.986798022879106895 ) ) ;
#1291=VERTEX_POINT ( 'NONE', #5748 ) ;
#1333=VERTEX_POINT ( 'NONE', #18288 ) ;
#1386=CARTESIAN_POINT ( 'NONE',  ( 52.34460878051607580, 78.91761970611439381, 26.32568957529414178 ) ) ;
#1395=DIRECTION ( 'NONE',  ( 1.000000000000000000, 0.000000000000000000, 0.000000000000000000 ) ) ;
#1400=EDGE_CURVE ( 'NONE', #8332, #15977, #20338, .T. ) ;
#1424=ORIENTED_EDGE ( 'NONE', *, *, #12432, .F. ) ;
#1459=AXIS2_PLACEMENT_3D ( 'NONE', #6860, #13886, #20874 ) ;
#1473=CARTESIAN_POINT ( 'NONE',  ( 109.7459976367008636, 75.42189990708665448, 7.816867676514023699 ) ) ;
#1487=FACE_BOUND ( 'NONE', #13024, .T. ) ;
#1490=EDGE_LOOP ( 'NONE', ( #11140, #6674, #21508, #8387 ) ) ;
#1500=VECTOR ( 'NONE', #10868, 1000.000000000000000 ) ;
#1677=CARTESIAN_POINT ( 'NONE',  ( 86.06478871700173272, 75.01038043515919185, -2.531004044634442174 ) ) ;
#1718=EDGE_CURVE ( 'NONE', #8332, #1333, #21667, .T. ) ;
#1779=CARTESIAN_POINT ( 'NONE',  ( 84.91452901814238885, 75.07584193902901859, -4.908336678377503759 ) ) ;
#1870=( LENGTH_UNIT ( ) NAMED_UNIT ( * ) SI_UNIT ( .MILLI., .METRE. ) );
#1894=CARTESIAN_POINT ( 'NONE',  ( 77.90572232234517003, 75.18523895546071856, -6.939197329751477739 ) ) ;
#1925=EDGE_CURVE ( 'NONE', #15977, #18898, #7876, .T. ) ;
#2114=CARTESIAN_POINT ( 'NONE',  ( 74.53966632203987785, 75.05140447157583594, -4.093706810995048961 ) ) ;
#2116=DIRECTION ( 'NONE',  ( 0.9999164797902015955, 2.001050586498092550E-22, -0.01292414190464117457 ) ) ;
#2124=ORIENTED_EDGE ( 'NONE', *, *, #20018, .T. ) ;
#2172=CLOSED_SHELL ( 'NONE', ( #244, #3472, #21006, #18530, #524, #2901, #10105, #7806 ) ) ;
#2215=PRODUCT_DEFINITION_FORMATION_WITH_SPECIFIED_SOURCE ( 'ANY', '', #19302, .NOT_KNOWN. ) ;
#2249=CARTESIAN_POINT ( 'NONE',  ( 74.41937658727354687, 75.03999983604417423, 1.800753062169240470 ) ) ;
#2317=CARTESIAN_POINT ( 'NONE',  ( 51.64670511766545502, 78.91761970611437960, -27.66980033337678790 ) ) ;
#2373=UNCERTAINTY_MEASURE_WITH_UNIT (LENGTH_MEASURE( 1.000000000000000082E-05 ), #4629, 'distance_accuracy_value', 'NONE');
#2405=ORIENTED_EDGE ( 'NONE', *, *, #20018, .F. ) ;
#2516=DIRECTION ( 'NONE',  ( 0.9999164797902015955, 2.001050586498092550E-22, -0.01292414190464117457 ) ) ;
#2717=CARTESIAN_POINT ( 'NONE',  ( 75.91984675752824785, 75.11612419797496898, 3.723726926507651580 ) ) ;
#2771=CARTESIAN_POINT ( 'NONE',  ( 51.64670511766545502, 84.99999999999997158, -27.66980033337678790 ) ) ;
#2830=ORIENTED_EDGE ( 'NONE', *, *, #1925, .T. ) ;
#2899=FACE_OUTER_BOUND ( 'NONE', #5109, .T. ) ;
#2901=ADVANCED_FACE ( 'NONE', ( #17215, #1487 ), #6756, .T. ) ;
#2924=CARTESIAN_POINT ( 'NONE',  ( 84.18163614557413155, 75.11642389258673802, 3.622972191343602155 ) ) ;
#3059=ORIENTED_EDGE ( 'NONE', *, *, #13281, .F. ) ;
#3102=CARTESIAN_POINT ( 'NONE',  ( 0.000000000000000000, 0.000000000000000000, 0.000000000000000000 ) ) ;
#3173=CARTESIAN_POINT ( 'NONE',  ( 106.9749367633763910, 78.91761970611439381, 25.61958048976759983 ) ) ;
#3284=CARTESIAN_POINT ( 'NONE',  ( 108.6468492096305596, 76.31988324137756763, -17.34982836191095146 ) ) ;
#3384=CARTESIAN_POINT ( 'NONE',  ( 86.24279638190517971, 74.99999999999998579, -1.114707239275309014 ) ) ;
#3389=APPLICATION_CONTEXT ( 'automotive_design' ) ;
#3472=ADVANCED_FACE ( 'NONE', ( #16083 ), #4096, .T. ) ;
#3603=CARTESIAN_POINT ( 'NONE',  ( 84.64642305175908632, 75.08946592368292272, -5.226459242126186844 ) ) ;
#3719=CARTESIAN_POINT ( 'NONE',  ( 76.62183188433269265, 75.14843384332513665, -6.300527722194164681 ) ) ;
#3843=CARTESIAN_POINT ( 'NONE',  ( 75.23002811022017511, 75.08930679774387329, -5.101340048736655142 ) ) ;
#3855=CARTESIAN_POINT ( 'NONE',  ( 106.9749367633763910, 184.8436277385793289, 25.61958048976753943 ) ) ;
#3955=CARTESIAN_POINT ( 'NONE',  ( 78.64967525538004622, 75.19535340807551904, 5.073326618873633009 ) ) ;
#4096=CYLINDRICAL_SURFACE ( 'NONE', #14326, 109.9999999999999716 ) ;
#4190=CARTESIAN_POINT ( 'NONE',  ( 73.97450750257705465, 75.01358823556745392, 0.6626198993681190474 ) ) ;
#4253=EDGE_LOOP ( 'NONE', ( #4264, #13895, #21323, #19303 ) ) ;
#4264=ORIENTED_EDGE ( 'NONE', *, *, #5813, .F. ) ;
#4411=CARTESIAN_POINT ( 'NONE',  ( 75.33668001145856863, 75.08929188680230027, 3.154648652659545860 ) ) ;
#4629=( LENGTH_UNIT ( ) NAMED_UNIT ( * ) SI_UNIT ( .MILLI., .METRE. ) );
#4640=CARTESIAN_POINT ( 'NONE',  ( 86.06165675176548291, 75.01312404301673098, 0.5177417398328088005 ) ) ;
#4655=CARTESIAN_POINT ( 'NONE',  ( 51.64670511766545502, 84.99999999999997158, -27.66980033337678790 ) ) ;
#4710=CARTESIAN_POINT ( 'NONE',  ( 52.34460878051607580, 78.91761970611439381, 26.32568957529414178 ) ) ;
#4725=CARTESIAN_POINT ( 'NONE',  ( 86.24279638190516550, 84.99999999999997158, -1.114707239275309458 ) ) ;
#4729=( NAMED_UNIT ( * ) PLANE_ANGLE_UNIT ( ) SI_UNIT ( $, .RADIAN. ) );
#4742=FACE_BOUND ( 'NONE', #13500, .T. ) ;
#4802=VECTOR ( 'NONE', #22498, 1000.000000000000114 ) ;
#4833=DIRECTION ( 'NONE',  ( -7.176269450075762180E-19, 1.000000000000000000, -5.550596000020001457E-17 ) ) ;
#4886=AXIS2_PLACEMENT_3D ( 'NONE', #7294, #75, #10418 ) ;
#4889=PRODUCT_DEFINITION_CONTEXT ( 'detailed design', #19944, 'design' ) ;
#4975=CARTESIAN_POINT ( 'NONE',  ( 86.24813375828298945, 75.00000000000002842, -0.7017644970498472246 ) ) ;
#5072=( NAMED_UNIT ( * ) SI_UNIT ( $, .STERADIAN. ) SOLID_ANGLE_UNIT ( ) );
#5109=EDGE_LOOP ( 'NONE', ( #3059, #14642, #22576, #2405 ) ) ;
#5115=CARTESIAN_POINT ( 'NONE',  ( 107.3521087218812369, 77.72700746170281150, -24.01651628897757007 ) ) ;
#5143=ORIENTED_EDGE ( 'NONE', *, *, #15467, .T. ) ;
#5195=EDGE_LOOP ( 'NONE', ( #6515, #7457, #20834, #19894 ) ) ;
#5233=ADVANCED_BREP_SHAPE_REPRESENTATION ( '', ( #9541, #6292 ), #13288 ) ;
#5324=CARTESIAN_POINT ( 'NONE',  ( 82.68550139462496418, 75.16567244870638831, -6.678086237966566863 ) ) ;
#5420=VECTOR ( 'NONE', #5787, 1000.000000000000000 ) ;
#5433=CARTESIAN_POINT ( 'NONE',  ( 78.29383429238851022, 75.19279626719429643, -7.062306694037421728 ) ) ;
#5438=B_SPLINE_CURVE_WITH_KNOTS ( 'NONE', 3,
 ( #3384, #14317, #7057, #1677, #8651, #22635, #6932, #17526, #9001, #1779, #3603, #8756, #15810, #53, #14087, #5324, #12363, #19344, #8887, #10616, #17639, #7175, #398, #12585, #5433, #1894, #14205, #21179, #19454, #3719, #282, #19568, #3843, #21284, #17882, #2114, #21611, #9705, #16386, #5896, #21837, #14545, #12931 ),
 .UNSPECIFIED., .F., .F.,
 ( 4, 2, 2, 2, 2, 2, 2, 2, 1, 2, 2, 2, 2, 2, 2, 2, 2, 2, 2, 2, 2, 4 ),
 ( 0.000000000000000000, 0.001221601669963557615, 0.001832402504945335664, 0.002443203339927113929, 0.003664805009890686072, 0.004886406679854257348, 0.006108008349817829058, 0.006718809184799614045, 0.007329610019781399900, 0.007940410854763185755, 0.008551211689744970743, 0.009772813359708502554, 0.01099441502967203263, 0.01221601669963556618, 0.01282681753461733035, 0.01343761836959909625, 0.01465922003956262980, 0.01588082170952616334, 0.01649162254450792231, 0.01710242337948967781, 0.01832402504945320962, 0.01954562671941673449 ),
 .UNSPECIFIED. ) ;
#5644=CARTESIAN_POINT ( 'NONE',  ( 51.64670511766545502, 78.91761970611437960, -27.66980033337678790 ) ) ;
#5667=CARTESIAN_POINT ( 'NONE',  ( 52.34460878051607580, 84.99999999999997158, 26.32568957529409204 ) ) ;
#5685=EDGE_CURVE ( 'NONE', #13983, #21156, #1016, .T. ) ;
#5748=CARTESIAN_POINT ( 'NONE',  ( 106.2770331005257702, 78.91761970611437960, -28.37590941890325880 ) ) ;
#5787=DIRECTION ( 'NONE',  ( 7.176269450075762180E-19, -1.000000000000000000, 5.550596000020001457E-17 ) ) ;
#5813=EDGE_CURVE ( 'NONE', #15229, #1291, #18902, .T. ) ;
#5896=CARTESIAN_POINT ( 'NONE',  ( 73.92355286441096496, 75.01302696078242604, -2.579009233597790107 ) ) ;
#5919=CARTESIAN_POINT ( 'NONE',  ( 74.72480678892256378, 75.05718735177460132, 2.334685081673636198 ) ) ;
#6237=DIRECTION ( 'NONE',  ( 0.9999164797902015955, 0.000000000000000000, -0.01292414190464118845 ) ) ;
#6268=CARTESIAN_POINT ( 'NONE',  ( 84.75118562858013149, 75.08956945039734876, 3.039329696154879024 ) ) ;
#6292=AXIS2_PLACEMENT_3D ( 'NONE', #3102, #12069, #1395 ) ;
#6515=ORIENTED_EDGE ( 'NONE', *, *, #15113, .F. ) ;
#6528=DIRECTION ( 'NONE',  ( 0.9999164797902017066, 2.001050586498416282E-22, -0.01292414190464117631 ) ) ;
#6674=ORIENTED_EDGE ( 'NONE', *, *, #20353, .F. ) ;
#6743=CARTESIAN_POINT ( 'NONE',  ( 110.0057602926817424, 75.00002486432201465, -0.2635329904031751269 ) ) ;
#6756=CYLINDRICAL_SURFACE ( 'NONE', #1459, 95.00000000000000000 ) ;
#6803=CARTESIAN_POINT ( 'NONE',  ( 73.74384038452764401, 84.99999999999997158, -0.9531554654672952376 ) ) ;
#6849=CARTESIAN_POINT ( 'NONE',  ( 108.2664294940537530, 76.72841911532559322, -19.58316954391773734 ) ) ;
#6860=CARTESIAN_POINT ( 'NONE',  ( 51.99565694909076541, 169.9999999999999716, -0.6720553790413538175 ) ) ;
#6895=ORIENTED_EDGE ( 'NONE', *, *, #1400, .F. ) ;
#6932=CARTESIAN_POINT ( 'NONE',  ( 85.81624039914329671, 75.02539222853825152, -3.313852530756491888 ) ) ;
#6963=CARTESIAN_POINT ( 'NONE',  ( 110.0024317885484635, 75.02128446332422129, 0.8997087025338614819 ) ) ;
#7057=CARTESIAN_POINT ( 'NONE',  ( 86.19166422048218124, 75.00269207195897536, -1.933333109913331738 ) ) ;
#7155=FILL_AREA_STYLE ('',( #20929 ) ) ;
#7175=CARTESIAN_POINT ( 'NONE',  ( 80.32251751971472231, 75.20580539967184563, -7.288561962794373628 ) ) ;
#7227=DIRECTION ( 'NONE',  ( -7.176269450075762180E-19, 1.000000000000000000, -5.550596000020001457E-17 ) ) ;
#7294=CARTESIAN_POINT ( 'NONE',  ( 51.99565694909076541, 169.9999999999999716, -0.6720553790413538175 ) ) ;
#7457=ORIENTED_EDGE ( 'NONE', *, *, #1718, .F. ) ;
#7472=PRODUCT_CONTEXT ( 'NONE', #3389, 'mechanical' ) ;
#7689=B_SPLINE_CURVE_WITH_KNOTS ( 'NONE', 3,
 ( #14678, #13073, #7877, #20037, #4190, #13176, #21630, #2249, #20141, #5919, #14917, #4411, #2717, #12955, #12719, #11220, #9250, #19686, #18227, #3955, #10978, #539, #18006, #8317, #18778, #1230, #11901, #15015, #10278, #13510, #20607, #2924, #6268, #20269, #10163, #13740, #15358, #20487, #20723, #4640, #22306, #4975, #16969 ),
 .UNSPECIFIED., .F., .F.,
 ( 4, 2, 2, 1, 2, 2, 2, 2, 2, 2, 2, 2, 2, 2, 2, 2, 2, 2, 2, 2, 2, 4 ),
 ( 0.01954562671941673449, 0.02076694801418337011, 0.02137760866156668618, 0.02198826930895000573, 0.02259892995633332180, 0.02320959060371664134, 0.02443091189848327349, 0.02565223319324991258, 0.02687355448801654473, 0.02748421513539988509, 0.02809487578278321851, 0.02931619707754989229, 0.03053751837231656954, 0.03114817901969990643, 0.03175883966708323985, 0.03298016096184991364, 0.03420148225661659436, 0.03542280355138326120, 0.03603346419876658768, 0.03664412484614991417, 0.03786544614091655325, 0.03908676743568318540 ),
 .UNSPECIFIED. ) ;
#7698=DIRECTION ( 'NONE',  ( 0.9999164797902015955, 0.000000000000000000, -0.01292414190464118845 ) ) ;
#7732=LINE ( 'NONE', #4710, #4802 ) ;
#7806=ADVANCED_FACE ( 'NONE', ( #21800 ), #11716, .F. ) ;
#7876=LINE ( 'NONE', #16297, #5420 ) ;
#7877=CARTESIAN_POINT ( 'NONE',  ( 73.79388979939501780, 75.00262671344128762, -0.1404264124762290289 ) ) ;
#8010=CARTESIAN_POINT ( 'NONE',  ( 73.74384038452764401, 74.99899999999998101, -0.9531554654672949045 ) ) ;
#8056=VECTOR ( 'NONE', #20300, 1000.000000000000000 ) ;
#8079=SHAPE_REPRESENTATION_RELATIONSHIP ( 'NONE' , 'NONE' ,  #21889, #5233 ) ;
#8097=PLANE ( 'NONE',  #15883 ) ;
#8221=FACE_OUTER_BOUND ( 'NONE', #5195, .T. ) ;
#8235=CARTESIAN_POINT ( 'NONE',  ( 52.34460878051607580, 84.99999999999997158, 26.32568957529409204 ) ) ;
#8243=CARTESIAN_POINT ( 'NONE',  ( 106.9749367633763910, 78.91761970611439381, 25.61958048976759983 ) ) ;
#8317=CARTESIAN_POINT ( 'NONE',  ( 80.88825763458693530, 75.20315502959410026, 5.165049547085412307 ) ) ;
#8332=VERTEX_POINT ( 'NONE', #11939 ) ;
#8339=AXIS2_PLACEMENT_3D ( 'NONE', #1075, #4833, #6237 ) ;
#8387=ORIENTED_EDGE ( 'NONE', *, *, #1718, .T. ) ;
#8452=CARTESIAN_POINT ( 'NONE',  ( 109.9190928854304588, 75.16976796352440715, 4.372055995853181720 ) ) ;
#8478=PLANE ( 'NONE',  #22581 ) ;
#8484=DIRECTION ( 'NONE',  ( 0.9999164797902015955, 0.000000000000000000, -0.01292414190464118845 ) ) ;
#8571=CARTESIAN_POINT ( 'NONE',  ( 108.0150042066416347, 77.63434920764957781, 21.27676351751525274 ) ) ;
#8651=CARTESIAN_POINT ( 'NONE',  ( 86.01272713495869482, 75.01355197838040567, -2.728429179322157783 ) ) ;
#8674=CARTESIAN_POINT ( 'NONE',  ( 106.2770331005257702, 78.91761970611437960, -28.37590941890325880 ) ) ;
#8702=ORIENTED_EDGE ( 'NONE', *, *, #17652, .F. ) ;
#8756=CARTESIAN_POINT ( 'NONE',  ( 84.06242043834124900, 75.11631364573369751, -5.795347279148256980 ) ) ;
#8780=VECTOR ( 'NONE', #866, 1000.000000000000114 ) ;
#8794=VERTEX_POINT ( 'NONE', #17090 ) ;
#8863=EDGE_CURVE ( 'NONE', #1291, #1333, #15593, .T. ) ;
#8887=CARTESIAN_POINT ( 'NONE',  ( 81.53656681450840438, 75.19215068228483290, -7.093857522514749547 ) ) ;
#8989=UNCERTAINTY_MEASURE_WITH_UNIT (LENGTH_MEASURE( 1.000000000000000082E-05 ), #1870, 'distance_accuracy_value', 'NONE');
#9001=CARTESIAN_POINT ( 'NONE',  ( 85.37691781808469216, 75.05100517808324412, -4.234898060786123963 ) ) ;
#9013=LINE ( 'NONE', #3855, #1500 ) ;
#9250=CARTESIAN_POINT ( 'NONE',  ( 77.86064527566928462, 75.18028080999435758, 4.844510309476128818 ) ) ;
#9259=AXIS2_PLACEMENT_3D ( 'NONE', #13082, #1002, #14810 ) ;
#9296=CIRCLE ( 'NONE', #4886, 95.00000000000000000 ) ;
#9316=LINE ( 'NONE', #2317, #17043 ) ;
#9338=CIRCLE ( 'NONE', #22159, 6.250000000000000000 ) ;
#9388=DIRECTION ( 'NONE',  ( 7.176269450075762180E-19, -1.000000000000000000, 5.550596000020001457E-17 ) ) ;
#9445=VECTOR ( 'NONE', #17031, 1000.000000000000227 ) ;
#9504=DIRECTION ( 'NONE',  ( 0.9999164797902017066, 0.000000000000000000, -0.01292414190464117631 ) ) ;
#9541=MANIFOLD_SOLID_BREP ( 'Stock-MAS-425-1', #2172 ) ;
#9635=CIRCLE ( 'NONE', #448, 109.9999999999999716 ) ;
#9705=CARTESIAN_POINT ( 'NONE',  ( 74.26458564358016190, 75.03487962395588795, -3.541144389642402857 ) ) ;
#9880=CARTESIAN_POINT ( 'NONE',  ( 106.9749367633763910, 84.99999999999997158, 25.61958048976753943 ) ) ;
#9913=CARTESIAN_POINT ( 'NONE',  ( 86.24279638190516550, 74.99899999999998101, -1.114707239275309014 ) ) ;
#10105=ADVANCED_FACE ( 'NONE', ( #22235 ), #14949, .F. ) ;
#10163=CARTESIAN_POINT ( 'NONE',  ( 85.34197260657376205, 75.05748221035003098, 2.205900974544971138 ) ) ;
#10196=CARTESIAN_POINT ( 'NONE',  ( 108.7959396947362478, 76.66003400751192487, 16.85290706162241037 ) ) ;
#10209=ORIENTED_EDGE ( 'NONE', *, *, #15467, .F. ) ;
#10278=CARTESIAN_POINT ( 'NONE',  ( 82.83339755747347510, 75.16617595114340133, 4.548589192762809041 ) ) ;
#10418=DIRECTION ( 'NONE',  ( -0.01292414190464115722, 0.000000000000000000, -0.9999164797902015955 ) ) ;
#10616=CARTESIAN_POINT ( 'NONE',  ( 81.33532363055485348, 75.19538212720385673, -7.141617114204432681 ) ) ;
#10868=DIRECTION ( 'NONE',  ( 7.176269450075762180E-19, -1.000000000000000000, 5.550596000020001457E-17 ) ) ;
#10875=ORIENTED_EDGE ( 'NONE', *, *, #11871, .F. ) ;
#10890=DIRECTION ( 'NONE',  ( -0.9999164797902017066, 0.000000000000000000, 0.01292414190464117631 ) ) ;
#10978=CARTESIAN_POINT ( 'NONE',  ( 79.25033911284278076, 75.20308137605636034, 5.185103052828717196 ) ) ;
#11050=EDGE_CURVE ( 'NONE', #8794, #13983, #5438, .T. ) ;
#11140=ORIENTED_EDGE ( 'NONE', *, *, #8863, .F. ) ;
#11220=CARTESIAN_POINT ( 'NONE',  ( 77.29073663370949987, 75.16594760505751083, 4.616381533551536798 ) ) ;
#11257=CARTESIAN_POINT ( 'NONE',  ( 51.99565694909076541, 169.9999999999999716, -0.6720553790413538175 ) ) ;
#11454=VECTOR ( 'NONE', #20289, 1000.000000000000000 ) ;
#11716=CYLINDRICAL_SURFACE ( 'NONE', #16992, 6.250000000000000000 ) ;
#11871=EDGE_CURVE ( 'NONE', #21156, #21267, #9338, .T. ) ;
#11901=CARTESIAN_POINT ( 'NONE',  ( 82.07389037140740129, 75.18483361449105473, 4.863163123076542860 ) ) ;
#11927=LINE ( 'NONE', #4655, #11454 ) ;
#11939=CARTESIAN_POINT ( 'NONE',  ( 51.64670511766545502, 84.99999999999997158, -27.66980033337678790 ) ) ;
#12036=ORIENTED_EDGE ( 'NONE', *, *, #5813, .T. ) ;
#12069=DIRECTION ( 'NONE',  ( 0.000000000000000000, 0.000000000000000000, 1.000000000000000000 ) ) ;
#12106=SURFACE_STYLE_FILL_AREA ( #7155 ) ;
#12150=CARTESIAN_POINT ( 'NONE',  ( 106.8378915622753880, 78.29428632475668337, -26.20941106207498095 ) ) ;
#12363=CARTESIAN_POINT ( 'NONE',  ( 82.31479625729774341, 75.17608775817923572, -6.847477558719483604 ) ) ;
#12432=EDGE_CURVE ( 'NONE', #21267, #21156, #19895, .T. ) ;
#12585=CARTESIAN_POINT ( 'NONE',  ( 79.09341253102171265, 75.20311826365394836, -7.232296047367152703 ) ) ;
#12587=DIRECTION ( 'NONE',  ( 0.01292414190464117631, 5.551059884324762197E-17, 0.9999164797902017066 ) ) ;
#12719=CARTESIAN_POINT ( 'NONE',  ( 76.92953810531172110, 75.15462563255036343, 4.428914867104452036 ) ) ;
#12917=EDGE_LOOP ( 'NONE', ( #5143, #12036, #1160, #14907 ) ) ;
#12931=CARTESIAN_POINT ( 'NONE',  ( 73.74384038452764401, 74.99999999999998579, -0.9531554654672949045 ) ) ;
#12955=CARTESIAN_POINT ( 'NONE',  ( 76.24440817582265595, 75.12974839299529606, 3.983549157388267759 ) ) ;
#13024=EDGE_LOOP ( 'NONE', ( #18296, #13871 ) ) ;
#13045=MECHANICAL_DESIGN_GEOMETRIC_PRESENTATION_REPRESENTATION('',(#18876),#22173);
#13073=CARTESIAN_POINT ( 'NONE',  ( 73.74911173825391586, 74.99999999999995737, -0.5453207712484345882 ) ) ;
#13082=CARTESIAN_POINT ( 'NONE',  ( 79.99331838321640475, 84.99999999999997158, -1.033931352371301848 ) ) ;
#13092=CARTESIAN_POINT ( 'NONE',  ( 2.775557561562891351E-13, 84.99999999999997158, 4.271756559592887470E-14 ) ) ;
#13151=EDGE_CURVE ( 'NONE', #18898, #1217, #9296, .T. ) ;
#13176=CARTESIAN_POINT ( 'NONE',  ( 74.09836678676883537, 75.02106928012277365, 1.052672645090043879 ) ) ;
#13281=EDGE_CURVE ( 'NONE', #13983, #8794, #7689, .T. ) ;
#13288=( GEOMETRIC_REPRESENTATION_CONTEXT ( 3 ) GLOBAL_UNCERTAINTY_ASSIGNED_CONTEXT ( ( #2373 ) ) GLOBAL_UNIT_ASSIGNED_CONTEXT ( ( #4629, #4729, #13606 ) ) REPRESENTATION_CONTEXT ( 'NONE', 'WORKASPACE' ) );
#13500=EDGE_LOOP ( 'NONE', ( #1424, #10875 ) ) ;
#13510=CARTESIAN_POINT ( 'NONE',  ( 83.18996550559461411, 75.15486823347328027, 4.352207832899844142 ) ) ;
#13606=( NAMED_UNIT ( * ) SI_UNIT ( $, .STERADIAN. ) SOLID_ANGLE_UNIT ( ) );
#13686=EDGE_LOOP ( 'NONE', ( #10209, #8702, #2830, #17289 ) ) ;
#13724=SURFACE_SIDE_STYLE ('',( #12106 ) ) ;
#13740=CARTESIAN_POINT ( 'NONE',  ( 85.44631271373334869, 75.05144267248711287, 2.026989630736137471 ) ) ;
#13767=CARTESIAN_POINT ( 'NONE',  ( 109.9311545250608617, 74.99990065235996894, -6.043940776851986385 ) ) ;
#13842=DIRECTION ( 'NONE',  ( 0.9999164797902015955, 2.001050586498092550E-22, -0.01292414190464117457 ) ) ;
#13870=CARTESIAN_POINT ( 'NONE',  ( 107.5937258339208142, 77.46195535017201905, -22.91004653791229018 ) ) ;
#13871=ORIENTED_EDGE ( 'NONE', *, *, #13281, .T. ) ;
#13886=DIRECTION ( 'NONE',  ( 0.9999164797902017066, 2.001050586498092786E-22, -0.01292414190464117631 ) ) ;
#13895=ORIENTED_EDGE ( 'NONE', *, *, #21417, .F. ) ;
#13947=PRODUCT_DEFINITION ( 'UNKNOWN', '', #2215, #4889 ) ;
#13964=CARTESIAN_POINT ( 'NONE',  ( 106.2770331005257276, 184.8436277385793289, -28.37590941890332985 ) ) ;
#13983=VERTEX_POINT ( 'NONE', #22601 ) ;
#14087=CARTESIAN_POINT ( 'NONE',  ( 83.04875907314333006, 75.15446773302494421, -6.489993662301849930 ) ) ;
#14203=PRODUCT_DEFINITION_SHAPE ( 'NONE', 'NONE',  #13947 ) ;
#14205=CARTESIAN_POINT ( 'NONE',  ( 77.34116450907883689, 75.17093467388001216, -6.697014498691808981 ) ) ;
#14317=CARTESIAN_POINT ( 'NONE',  ( 86.23745778024132846, 74.99999999999998579, -1.527744779571642342 ) ) ;
#14326=AXIS2_PLACEMENT_3D ( 'NONE', #442, #9388, #10890 ) ;
#14334=ORIENTED_EDGE ( 'NONE', *, *, #11050, .F. ) ;
#14545=CARTESIAN_POINT ( 'NONE',  ( 73.73856782067191773, 74.99999999999998579, -1.361083785117223499 ) ) ;
#14642=ORIENTED_EDGE ( 'NONE', *, *, #5685, .T. ) ;
#14678=CARTESIAN_POINT ( 'NONE',  ( 73.74384038452764401, 74.99999999999998579, -0.9531554654672949045 ) ) ;
#14778=CARTESIAN_POINT ( 'NONE',  ( 52.34460878051607580, 84.99999999999997158, 26.32568957529409204 ) ) ;
#14810=DIRECTION ( 'NONE',  ( 0.9999164797902015955, 0.000000000000000000, -0.01292414190464118845 ) ) ;
#14872=AXIS2_PLACEMENT_3D ( 'NONE', #5667, #12587, #2116 ) ;
#14907=ORIENTED_EDGE ( 'NONE', *, *, #15113, .T. ) ;
#14917=CARTESIAN_POINT ( 'NONE',  ( 75.07406019263973462, 75.07594612489205588, 2.843253612283983767 ) ) ;
#14919=ORIENTED_EDGE ( 'NONE', *, *, #5685, .F. ) ;
#14949=PLANE ( 'NONE',  #20366 ) ;
#14991=ORIENTED_EDGE ( 'NONE', *, *, #15159, .F. ) ;
#15015=CARTESIAN_POINT ( 'NONE',  ( 82.26820226798385249, 75.18049222980359048, 4.790965612300991161 ) ) ;
#15113=EDGE_CURVE ( 'NONE', #1333, #558, #9635, .T. ) ;
#15159=EDGE_CURVE ( 'NONE', #1217, #8332, #11927, .T. ) ;
#15229=VERTEX_POINT ( 'NONE', #8243 ) ;
#15358=CARTESIAN_POINT ( 'NONE',  ( 85.63487699384957352, 75.04022993534840680, 1.663697398266591909 ) ) ;
#15467=EDGE_CURVE ( 'NONE', #558, #15229, #9013, .T. ) ;
#15502=CARTESIAN_POINT ( 'NONE',  ( 109.9590233273770679, 75.10625493178588385, 3.218332492612444362 ) ) ;
#15578=CARTESIAN_POINT ( 'NONE',  ( 51.64670511766545502, 84.99999999999997158, -27.66980033337678790 ) ) ;
#15593=LINE ( 'NONE', #13964, #18015 ) ;
#15810=CARTESIAN_POINT ( 'NONE',  ( 83.74446663462045137, 75.12966630363247589, -6.049935108198452482 ) ) ;
#15812=PLANE ( 'NONE',  #14872 ) ;
#15883=AXIS2_PLACEMENT_3D ( 'NONE', #15578, #22084, #13842 ) ;
#15977=VERTEX_POINT ( 'NONE', #8235 ) ;
#15992=CARTESIAN_POINT ( 'NONE',  ( 79.99331838321640475, 84.99999999999997158, -1.033931352371301848 ) ) ;
#16083=FACE_OUTER_BOUND ( 'NONE', #12917, .T. ) ;
#16116=ORIENTED_EDGE ( 'NONE', *, *, #1925, .F. ) ;
#16297=CARTESIAN_POINT ( 'NONE',  ( 52.34460878051607580, 84.99999999999997158, 26.32568957529409204 ) ) ;
#16386=CARTESIAN_POINT ( 'NONE',  ( 74.03668283561377450, 75.02057536297186857, -2.970158874850576947 ) ) ;
#16458=CARTESIAN_POINT ( 'NONE',  ( 79.99331838321640475, 74.99899999999998101, -1.033931352371301404 ) ) ;
#16969=CARTESIAN_POINT ( 'NONE',  ( 86.24279638190517971, 74.99999999999998579, -1.114707239275309014 ) ) ;
#16992=AXIS2_PLACEMENT_3D ( 'NONE', #16458, #705, #7698 ) ;
#17031=DIRECTION ( 'NONE',  ( 0.01292414190464117631, 5.551059884324760964E-17, 0.9999164797902015955 ) ) ;
#17043=VECTOR ( 'NONE', #19982, 1000.000000000000114 ) ;
#17090=CARTESIAN_POINT ( 'NONE',  ( 86.24279638190517971, 74.99999999999998579, -1.114707239275309014 ) ) ;
#17181=VECTOR ( 'NONE', #2516, 1000.000000000000114 ) ;
#17215=FACE_OUTER_BOUND ( 'NONE', #4253, .T. ) ;
#17289=ORIENTED_EDGE ( 'NONE', *, *, #21417, .T. ) ;
#17443=CARTESIAN_POINT ( 'NONE',  ( 106.5651016638878446, 78.59671595044419234, -27.29699872068776401 ) ) ;
#17526=CARTESIAN_POINT ( 'NONE',  ( 85.57356156445646889, 75.03970044275367002, -3.878440373465425139 ) ) ;
#17639=CARTESIAN_POINT ( 'NONE',  ( 80.72863657406642801, 75.20316443938568796, -7.254142036499096946 ) ) ;
#17652=EDGE_CURVE ( 'NONE', #15977, #558, #17985, .T. ) ;
#17749=( NAMED_UNIT ( * ) PLANE_ANGLE_UNIT ( ) SI_UNIT ( $, .RADIAN. ) );
#17882=CARTESIAN_POINT ( 'NONE',  ( 74.64244246480362222, 75.05735400057622542, -4.269988455633038527 ) ) ;
#17985=LINE ( 'NONE', #14778, #8780 ) ;
#18006=CARTESIAN_POINT ( 'NONE',  ( 80.48140932536705350, 75.20583697296392245, 5.210614517255996780 ) ) ;
#18015=VECTOR ( 'NONE', #20955, 1000.000000000000000 ) ;
#18227=CARTESIAN_POINT ( 'NONE',  ( 78.45092939588570857, 75.19216699751922306, 5.026242266752571020 ) ) ;
#18263=DIRECTION ( 'NONE',  ( -0.01292414190464117457, -5.551059884324760964E-17, -0.9999164797902015955 ) ) ;
#18288=CARTESIAN_POINT ( 'NONE',  ( 106.2770331005257134, 84.99999999999997158, -28.37590941890332985 ) ) ;
#18296=ORIENTED_EDGE ( 'NONE', *, *, #11050, .T. ) ;
#18530=ADVANCED_FACE ( 'NONE', ( #8221, #4742 ), #8097, .T. ) ;
#18539=LINE ( 'NONE', #9913, #519 ) ;
#18778=CARTESIAN_POINT ( 'NONE',  ( 81.48578126947279543, 75.19548211375456503, 5.038671026100010053 ) ) ;
#18876=STYLED_ITEM ( 'NONE', ( #19434 ), #9541 ) ;
#18880=EDGE_LOOP ( 'NONE', ( #14919, #14334, #2124, #20068 ) ) ;
#18898=VERTEX_POINT ( 'NONE', #1386 ) ;
#18902=B_SPLINE_CURVE_WITH_KNOTS ( 'NONE', 3,
 ( #3173, #8571, #10196, #22557, #1473, #8452, #15502, #6963, #6743, #13767, #19022, #3284, #6849, #13870, #5115, #12150, #17443, #8674 ),
 .UNSPECIFIED., .F., .F.,
 ( 4, 2, 2, 2, 2, 2, 2, 2, 4 ),
 ( 3.469446951953613804E-18, 0.01374954366077128440, 0.02062431549115692139, 0.02406170140634973989, 0.02749908732154255492, 0.04124863098231382197, 0.04812340281269945202, 0.05156078872789227746, 0.05499817464308508902 ),
 .UNSPECIFIED. ) ;
#18945=CARTESIAN_POINT ( 'NONE',  ( 51.64670511766545502, 84.99999999999997158, -27.66980033337678790 ) ) ;
#19022=CARTESIAN_POINT ( 'NONE',  ( 109.5818730699487560, 75.33563225513333350, -10.60333173834208687 ) ) ;
#19302=PRODUCT ( 'Angle Locking Side Clamp', 'Angle Locking Side Clamp', '', ( #7472 ) ) ;
#19303=ORIENTED_EDGE ( 'NONE', *, *, #20353, .T. ) ;
#19344=CARTESIAN_POINT ( 'NONE',  ( 81.92940647337731264, 75.18465056264352597, -6.980012735552315384 ) ) ;
#19434=PRESENTATION_STYLE_ASSIGNMENT (( #22515 ) ) ;
#19454=CARTESIAN_POINT ( 'NONE',  ( 76.79553162410384459, 75.15439084847217543, -6.407829649116825621 ) ) ;
#19568=CARTESIAN_POINT ( 'NONE',  ( 75.80607982450202087, 75.11648168028638395, -5.692233723461522565 ) ) ;
#19686=CARTESIAN_POINT ( 'NONE',  ( 78.05646167423948611, 75.18463598142704996, 4.911928902550189768 ) ) ;
#19825=DIRECTION ( 'NONE',  ( 7.176269450075763143E-19, -1.000000000000000000, 5.550596000020002074E-17 ) ) ;
#19848=EDGE_LOOP ( 'NONE', ( #16116, #6895, #14991, #21265 ) ) ;
#19894=ORIENTED_EDGE ( 'NONE', *, *, #17652, .T. ) ;
#19895=CIRCLE ( 'NONE', #9259, 6.250000000000000000 ) ;
#19944=APPLICATION_CONTEXT ( 'automotive_design' ) ;
#19966=COLOUR_RGB ( '', 0.66274510, 0.83137255, 0.94901961) ;
#19982=DIRECTION ( 'NONE',  ( 0.9999164797902015955, 2.001050586498092550E-22, -0.01292414190464117457 ) ) ;
#20018=EDGE_CURVE ( 'NONE', #8794, #21267, #18539, .T. ) ;
#20037=CARTESIAN_POINT ( 'NONE',  ( 73.92160891109067222, 75.01036581836726214, 0.4624093665085752813 ) ) ;
#20068=ORIENTED_EDGE ( 'NONE', *, *, #12432, .T. ) ;
#20141=CARTESIAN_POINT ( 'NONE',  ( 74.61645886759328050, 75.05117449683021391, 2.158817404397858297 ) ) ;
#20269=CARTESIAN_POINT ( 'NONE',  ( 85.00589227782222679, 75.07622562672395361, 2.721739690384933130 ) ) ;
#20289=DIRECTION ( 'NONE',  ( -7.176269450075762180E-19, 1.000000000000000000, -5.550596000020001457E-17 ) ) ;
#20300=DIRECTION ( 'NONE',  ( -7.176269450075762180E-19, 1.000000000000000000, -5.550596000020001457E-17 ) ) ;
#20338=LINE ( 'NONE', #18945, #9445 ) ;
#20353=EDGE_CURVE ( 'NONE', #1217, #1291, #9316, .T. ) ;
#20366=AXIS2_PLACEMENT_3D ( 'NONE', #11257, #6528, #18263 ) ;
#20487=CARTESIAN_POINT ( 'NONE',  ( 85.71976348773939947, 75.03502047313104129, 1.478386053088734053 ) ) ;
#20607=CARTESIAN_POINT ( 'NONE',  ( 83.86322835067295500, 75.13004950108779667, 3.890786405216685839 ) ) ;
#20667=FACE_OUTER_BOUND ( 'NONE', #1490, .T. ) ;
#20723=CARTESIAN_POINT ( 'NONE',  ( 85.94671339373330454, 75.02078408288856792, 0.9116371949491822724 ) ) ;
#20834=ORIENTED_EDGE ( 'NONE', *, *, #1400, .T. ) ;
#20874=DIRECTION ( 'NONE',  ( -0.01292414190464115722, 0.000000000000000000, -0.9999164797902015955 ) ) ;
#20929=FILL_AREA_STYLE_COLOUR ( '', #19966 ) ;
#20955=DIRECTION ( 'NONE',  ( -7.176269450075762180E-19, 1.000000000000000000, -5.550596000020001457E-17 ) ) ;
#21006=ADVANCED_FACE ( 'NONE', ( #21402 ), #15812, .T. ) ;
#21156=VERTEX_POINT ( 'NONE', #6803 ) ;
#21179=CARTESIAN_POINT ( 'NONE',  ( 77.15497946248154904, 75.16563907528397692, -6.606045424387566811 ) ) ;
#21265=ORIENTED_EDGE ( 'NONE', *, *, #13151, .F. ) ;
#21267=VERTEX_POINT ( 'NONE', #4725 ) ;
#21284=CARTESIAN_POINT ( 'NONE',  ( 74.97531732193478149, 75.07593137031709318, -4.781986851995010390 ) ) ;
#21323=ORIENTED_EDGE ( 'NONE', *, *, #13151, .T. ) ;
#21402=FACE_OUTER_BOUND ( 'NONE', #13686, .T. ) ;
#21417=EDGE_CURVE ( 'NONE', #18898, #15229, #7732, .T. ) ;
#21508=ORIENTED_EDGE ( 'NONE', *, *, #15159, .T. ) ;
#21611=CARTESIAN_POINT ( 'NONE',  ( 74.35083714549891454, 75.04017415462969609, -3.729659851975327900 ) ) ;
#21630=CARTESIAN_POINT ( 'NONE',  ( 74.24069787013584687, 75.02961117147833647, 1.434652486052601983 ) ) ;
#21667=LINE ( 'NONE', #461, #17181 ) ;
#21800=FACE_OUTER_BOUND ( 'NONE', #18880, .T. ) ;
#21837=CARTESIAN_POINT ( 'NONE',  ( 73.77409342887030164, 75.00271445951732119, -1.775928710569730340 ) ) ;
#21889=SHAPE_REPRESENTATION ( 'Angle Locking Side Clamp', ( #6292 ), #13288 ) ;
#22029=DIRECTION ( 'NONE',  ( -0.01292414190464117631, -5.551059884324762197E-17, -0.9999164797902017066 ) ) ;
#22084=DIRECTION ( 'NONE',  ( -7.176269450075758328E-19, 1.000000000000000000, -5.550596000020002074E-17 ) ) ;
#22149=DIRECTION ( 'NONE',  ( -0.9999164797902015955, -2.001050586498092550E-22, 0.01292414190464117457 ) ) ;
#22159=AXIS2_PLACEMENT_3D ( 'NONE', #15992, #7227, #8484 ) ;
#22173=( GEOMETRIC_REPRESENTATION_CONTEXT ( 3 ) GLOBAL_UNCERTAINTY_ASSIGNED_CONTEXT ( ( #8989 ) ) GLOBAL_UNIT_ASSIGNED_CONTEXT ( ( #1870, #17749, #5072 ) ) REPRESENTATION_CONTEXT ( 'NONE', 'WORKASPACE' ) );
#22182=DIRECTION ( 'NONE',  ( -7.176269450075762180E-19, 1.000000000000000000, -5.550596000020001457E-17 ) ) ;
#22235=FACE_OUTER_BOUND ( 'NONE', #19848, .T. ) ;
#22306=CARTESIAN_POINT ( 'NONE',  ( 86.21288355311105533, 75.00269236436724896, -0.2926965463156551706 ) ) ;
#22498=DIRECTION ( 'NONE',  ( 0.9999164797902015955, 2.001050586498092550E-22, -0.01292414190464117457 ) ) ;
#22515=SURFACE_STYLE_USAGE ( .BOTH. , #13724 ) ;
#22557=CARTESIAN_POINT ( 'NONE',  ( 109.5595887168318114, 75.67202325895546267, 10.09161844407532982 ) ) ;
#22576=ORIENTED_EDGE ( 'NONE', *, *, #11871, .T. ) ;
#22581=AXIS2_PLACEMENT_3D ( 'NONE', #2771, #22029, #22149 ) ;
#22601=CARTESIAN_POINT ( 'NONE',  ( 73.74384038452764401, 74.99999999999998579, -0.9531554654672949045 ) ) ;
#22635=CARTESIAN_POINT ( 'NONE',  ( 85.88862024204405543, 75.02104826936582072, -3.119601652154077254 ) ) ;
ENDSEC;
END-ISO-10303-21;
